ISO-10303-21;
HEADER;
/* Generated by software containing ST-Developer
 * from STEP Tools, Inc. (www.steptools.com) 
 */

FILE_DESCRIPTION(
/* description */ ('Swing-away clamp arm'),
/* implementation_level */ '2;1');

FILE_NAME(
/* name */ 'Cap Screw - M4x16.step',
/* time_stamp */ '2026-10-28T03:26:03-07:00',
/* author */ (''),
/* organization */ (''),
/* preprocessor_version */ 'ST-DEVELOPER v20.2',
/* originating_system */ 'Autodesk Translation Framework v15.17.0.0',
/* authorisation */ '');

FILE_SCHEMA (('AUTOMOTIVE_DESIGN { 1 0 10303 214 3 1 1 }'));
ENDSEC;

DATA;
#10=MECHANICAL_DESIGN_GEOMETRIC_PRESENTATION_REPRESENTATION('',(#325),#10627);
#208=CONICAL_SURFACE('',#5795,0.325,0.785398163397448);
#209=CONICAL_SURFACE('',#5799,0.335,0.785398163397448);
#210=CONICAL_SURFACE('',#5803,0.21,0.463647609000806);
#211=CONICAL_SURFACE('',#5807,0.18,0.785398163397448);
#216=ORIENTED_CLOSED_SHELL('',*,#4933,.F.);
#219=BREP_WITH_VOIDS('Body1',#4932,(#216));
#265=SHAPE_REPRESENTATION_RELATIONSHIP('SRR','None',#10766,#291);
#291=ADVANCED_BREP_SHAPE_REPRESENTATION('',(#219),#10625);
#325=STYLED_ITEM('',(#10972),#219);
#456=FACE_BOUND('',#1321,.T.);
#615=PLANE('',#5793);
#616=PLANE('',#5801);
#617=PLANE('',#5809);
#618=PLANE('',#5810);
#619=PLANE('',#5811);
#620=PLANE('',#5812);
#621=PLANE('',#5813);
#622=PLANE('',#5814);
#623=PLANE('',#5815);
#624=PLANE('',#5816);
#625=PLANE('',#5817);
#911=FACE_OUTER_BOUND('',#1316,.T.);
#912=FACE_OUTER_BOUND('',#1317,.T.);
#913=FACE_OUTER_BOUND('',#1318,.T.);
#914=FACE_OUTER_BOUND('',#1319,.T.);
#915=FACE_OUTER_BOUND('',#1320,.T.);
#916=FACE_OUTER_BOUND('',#1322,.T.);
#917=FACE_OUTER_BOUND('',#1323,.T.);
#918=FACE_OUTER_BOUND('',#1324,.T.);
#919=FACE_OUTER_BOUND('',#1325,.T.);
#920=FACE_OUTER_BOUND('',#1326,.T.);
#921=FACE_OUTER_BOUND('',#1327,.T.);
#922=FACE_OUTER_BOUND('',#1328,.T.);
#923=FACE_OUTER_BOUND('',#1329,.T.);
#924=FACE_OUTER_BOUND('',#1330,.T.);
#925=FACE_OUTER_BOUND('',#1331,.T.);
#926=FACE_OUTER_BOUND('',#1332,.T.);
#927=FACE_OUTER_BOUND('',#1333,.T.);
#1316=EDGE_LOOP('',(#4373));
#1317=EDGE_LOOP('',(#4374,#4375,#4376,#4377));
#1318=EDGE_LOOP('',(#4378,#4379,#4380,#4381));
#1319=EDGE_LOOP('',(#4382,#4383,#4384,#4385));
#1320=EDGE_LOOP('',(#4386));
#1321=EDGE_LOOP('',(#4387));
#1322=EDGE_LOOP('',(#4388,#4389,#4390,#4391));
#1323=EDGE_LOOP('',(#4392,#4393,#4394,#4395));
#1324=EDGE_LOOP('',(#4396,#4397,#4398,#4399));
#1325=EDGE_LOOP('',(#4400));
#1326=EDGE_LOOP('',(#4401,#4402,#4403,#4404));
#1327=EDGE_LOOP('',(#4405,#4406,#4407,#4408));
#1328=EDGE_LOOP('',(#4409,#4410,#4411,#4412));
#1329=EDGE_LOOP('',(#4413,#4414,#4415,#4416));
#1330=EDGE_LOOP('',(#4417,#4418,#4419,#4420));
#1331=EDGE_LOOP('',(#4421,#4422,#4423,#4424));
#1332=EDGE_LOOP('',(#4425,#4426,#4427,#4428,#4429,#4430));
#1333=EDGE_LOOP('',(#4431,#4432,#4433,#4434,#4435,#4436));
#1626=LINE('',#10407,#1948);
#1627=LINE('',#10411,#1949);
#1628=LINE('',#10415,#1950);
#1629=LINE('',#10422,#1951);
#1630=LINE('',#10426,#1952);
#1631=LINE('',#10430,#1953);
#1632=LINE('',#10435,#1954);
#1633=LINE('',#10437,#1955);
#1634=LINE('',#10439,#1956);
#1635=LINE('',#10440,#1957);
#1636=LINE('',#10443,#1958);
#1637=LINE('',#10445,#1959);
#1638=LINE('',#10446,#1960);
#1639=LINE('',#10449,#1961);
#1640=LINE('',#10451,#1962);
#1641=LINE('',#10452,#1963);
#1642=LINE('',#10455,#1964);
#1643=LINE('',#10457,#1965);
#1644=LINE('',#10458,#1966);
#1645=LINE('',#10461,#1967);
#1646=LINE('',#10463,#1968);
#1647=LINE('',#10464,#1969);
#1648=LINE('',#10466,#1970);
#1649=LINE('',#10467,#1971);
#1948=VECTOR('',#7293,0.325);
#1949=VECTOR('',#7298,0.35);
#1950=VECTOR('',#7303,0.335);
#1951=VECTOR('',#7312,0.21);
#1952=VECTOR('',#7317,0.2);
#1953=VECTOR('',#7322,0.18);
#1954=VECTOR('',#7327,1.);
#1955=VECTOR('',#7328,1.);
#1956=VECTOR('',#7329,1.);
#1957=VECTOR('',#7330,1.);
#1958=VECTOR('',#7333,1.);
#1959=VECTOR('',#7334,1.);
#1960=VECTOR('',#7335,1.);
#1961=VECTOR('',#7338,1.);
#1962=VECTOR('',#7339,1.);
#1963=VECTOR('',#7340,1.);
#1964=VECTOR('',#7343,1.);
#1965=VECTOR('',#7344,1.);
#1966=VECTOR('',#7345,1.);
#1967=VECTOR('',#7348,1.);
#1968=VECTOR('',#7349,1.);
#1969=VECTOR('',#7350,1.);
#1970=VECTOR('',#7353,1.);
#1971=VECTOR('',#7354,1.);
#2247=CIRCLE('',#5794,0.3);
#2248=CIRCLE('',#5796,0.35);
#2249=CIRCLE('',#5798,0.35);
#2250=CIRCLE('',#5800,0.32);
#2251=CIRCLE('',#5802,0.22);
#2252=CIRCLE('',#5804,0.1954);
#2253=CIRCLE('',#5806,0.1954);
#2254=CIRCLE('',#5808,0.16);
#2634=VERTEX_POINT('',#10402);
#2635=VERTEX_POINT('',#10405);
#2636=VERTEX_POINT('',#10409);
#2637=VERTEX_POINT('',#10413);
#2638=VERTEX_POINT('',#10417);
#2639=VERTEX_POINT('',#10420);
#2640=VERTEX_POINT('',#10424);
#2641=VERTEX_POINT('',#10428);
#2642=VERTEX_POINT('',#10433);
#2643=VERTEX_POINT('',#10434);
#2644=VERTEX_POINT('',#10436);
#2645=VERTEX_POINT('',#10438);
#2646=VERTEX_POINT('',#10442);
#2647=VERTEX_POINT('',#10444);
#2648=VERTEX_POINT('',#10448);
#2649=VERTEX_POINT('',#10450);
#2650=VERTEX_POINT('',#10454);
#2651=VERTEX_POINT('',#10456);
#2652=VERTEX_POINT('',#10460);
#2653=VERTEX_POINT('',#10462);
#3219=EDGE_CURVE('',#2634,#2634,#2247,.T.);
#3220=EDGE_CURVE('',#2635,#2635,#2248,.T.);
#3221=EDGE_CURVE('',#2635,#2634,#1626,.T.);
#3222=EDGE_CURVE('',#2636,#2636,#2249,.T.);
#3223=EDGE_CURVE('',#2636,#2635,#1627,.T.);
#3224=EDGE_CURVE('',#2637,#2637,#2250,.T.);
#3225=EDGE_CURVE('',#2637,#2636,#1628,.T.);
#3226=EDGE_CURVE('',#2638,#2638,#2251,.T.);
#3227=EDGE_CURVE('',#2639,#2639,#2252,.F.);
#3228=EDGE_CURVE('',#2639,#2638,#1629,.T.);
#3229=EDGE_CURVE('',#2640,#2640,#2253,.F.);
#3230=EDGE_CURVE('',#2640,#2639,#1630,.T.);
#3231=EDGE_CURVE('',#2641,#2641,#2254,.T.);
#3232=EDGE_CURVE('',#2641,#2640,#1631,.T.);
#3233=EDGE_CURVE('',#2642,#2643,#1632,.T.);
#3234=EDGE_CURVE('',#2643,#2644,#1633,.T.);
#3235=EDGE_CURVE('',#2644,#2645,#1634,.T.);
#3236=EDGE_CURVE('',#2642,#2645,#1635,.T.);
#3237=EDGE_CURVE('',#2643,#2646,#1636,.T.);
#3238=EDGE_CURVE('',#2646,#2647,#1637,.T.);
#3239=EDGE_CURVE('',#2647,#2644,#1638,.T.);
#3240=EDGE_CURVE('',#2646,#2648,#1639,.T.);
#3241=EDGE_CURVE('',#2648,#2649,#1640,.T.);
#3242=EDGE_CURVE('',#2649,#2647,#1641,.T.);
#3243=EDGE_CURVE('',#2648,#2650,#1642,.T.);
#3244=EDGE_CURVE('',#2650,#2651,#1643,.T.);
#3245=EDGE_CURVE('',#2651,#2649,#1644,.T.);
#3246=EDGE_CURVE('',#2650,#2652,#1645,.T.);
#3247=EDGE_CURVE('',#2652,#2653,#1646,.T.);
#3248=EDGE_CURVE('',#2653,#2651,#1647,.T.);
#3249=EDGE_CURVE('',#2652,#2642,#1648,.T.);
#3250=EDGE_CURVE('',#2645,#2653,#1649,.T.);
#4373=ORIENTED_EDGE('',*,*,#3219,.F.);
#4374=ORIENTED_EDGE('',*,*,#3220,.F.);
#4375=ORIENTED_EDGE('',*,*,#3221,.T.);
#4376=ORIENTED_EDGE('',*,*,#3219,.T.);
#4377=ORIENTED_EDGE('',*,*,#3221,.F.);
#4378=ORIENTED_EDGE('',*,*,#3222,.F.);
#4379=ORIENTED_EDGE('',*,*,#3223,.T.);
#4380=ORIENTED_EDGE('',*,*,#3220,.T.);
#4381=ORIENTED_EDGE('',*,*,#3223,.F.);
#4382=ORIENTED_EDGE('',*,*,#3224,.F.);
#4383=ORIENTED_EDGE('',*,*,#3225,.T.);
#4384=ORIENTED_EDGE('',*,*,#3222,.T.);
#4385=ORIENTED_EDGE('',*,*,#3225,.F.);
#4386=ORIENTED_EDGE('',*,*,#3224,.T.);
#4387=ORIENTED_EDGE('',*,*,#3226,.F.);
#4388=ORIENTED_EDGE('',*,*,#3227,.F.);
#4389=ORIENTED_EDGE('',*,*,#3228,.T.);
#4390=ORIENTED_EDGE('',*,*,#3226,.T.);
#4391=ORIENTED_EDGE('',*,*,#3228,.F.);
#4392=ORIENTED_EDGE('',*,*,#3229,.F.);
#4393=ORIENTED_EDGE('',*,*,#3230,.T.);
#4394=ORIENTED_EDGE('',*,*,#3227,.T.);
#4395=ORIENTED_EDGE('',*,*,#3230,.F.);
#4396=ORIENTED_EDGE('',*,*,#3231,.F.);
#4397=ORIENTED_EDGE('',*,*,#3232,.T.);
#4398=ORIENTED_EDGE('',*,*,#3229,.T.);
#4399=ORIENTED_EDGE('',*,*,#3232,.F.);
#4400=ORIENTED_EDGE('',*,*,#3231,.T.);
#4401=ORIENTED_EDGE('',*,*,#3233,.T.);
#4402=ORIENTED_EDGE('',*,*,#3234,.T.);
#4403=ORIENTED_EDGE('',*,*,#3235,.T.);
#4404=ORIENTED_EDGE('',*,*,#3236,.F.);
#4405=ORIENTED_EDGE('',*,*,#3237,.T.);
#4406=ORIENTED_EDGE('',*,*,#3238,.T.);
#4407=ORIENTED_EDGE('',*,*,#3239,.T.);
#4408=ORIENTED_EDGE('',*,*,#3234,.F.);
#4409=ORIENTED_EDGE('',*,*,#3240,.T.);
#4410=ORIENTED_EDGE('',*,*,#3241,.T.);
#4411=ORIENTED_EDGE('',*,*,#3242,.T.);
#4412=ORIENTED_EDGE('',*,*,#3238,.F.);
#4413=ORIENTED_EDGE('',*,*,#3243,.T.);
#4414=ORIENTED_EDGE('',*,*,#3244,.T.);
#4415=ORIENTED_EDGE('',*,*,#3245,.T.);
#4416=ORIENTED_EDGE('',*,*,#3241,.F.);
#4417=ORIENTED_EDGE('',*,*,#3246,.T.);
#4418=ORIENTED_EDGE('',*,*,#3247,.T.);
#4419=ORIENTED_EDGE('',*,*,#3248,.T.);
#4420=ORIENTED_EDGE('',*,*,#3244,.F.);
#4421=ORIENTED_EDGE('',*,*,#3249,.T.);
#4422=ORIENTED_EDGE('',*,*,#3236,.T.);
#4423=ORIENTED_EDGE('',*,*,#3250,.T.);
#4424=ORIENTED_EDGE('',*,*,#3247,.F.);
#4425=ORIENTED_EDGE('',*,*,#3249,.F.);
#4426=ORIENTED_EDGE('',*,*,#3246,.F.);
#4427=ORIENTED_EDGE('',*,*,#3243,.F.);
#4428=ORIENTED_EDGE('',*,*,#3240,.F.);
#4429=ORIENTED_EDGE('',*,*,#3237,.F.);
#4430=ORIENTED_EDGE('',*,*,#3233,.F.);
#4431=ORIENTED_EDGE('',*,*,#3250,.F.);
#4432=ORIENTED_EDGE('',*,*,#3235,.F.);
#4433=ORIENTED_EDGE('',*,*,#3239,.F.);
#4434=ORIENTED_EDGE('',*,*,#3242,.F.);
#4435=ORIENTED_EDGE('',*,*,#3245,.F.);
#4436=ORIENTED_EDGE('',*,*,#3248,.F.);
#4588=CYLINDRICAL_SURFACE('',#5797,0.35);
#4589=CYLINDRICAL_SURFACE('',#5805,0.1954);
#4866=ADVANCED_FACE('',(#911),#615,.T.);
#4867=ADVANCED_FACE('',(#912),#208,.T.);
#4868=ADVANCED_FACE('',(#913),#4588,.T.);
#4869=ADVANCED_FACE('',(#914),#209,.T.);
#4870=ADVANCED_FACE('',(#915,#456),#616,.T.);
#4871=ADVANCED_FACE('',(#916),#210,.T.);
#4872=ADVANCED_FACE('',(#917),#4589,.T.);
#4873=ADVANCED_FACE('',(#918),#211,.T.);
#4874=ADVANCED_FACE('',(#919),#617,.T.);
#4875=ADVANCED_FACE('',(#920),#618,.F.);
#4876=ADVANCED_FACE('',(#921),#619,.F.);
#4877=ADVANCED_FACE('',(#922),#620,.F.);
#4878=ADVANCED_FACE('',(#923),#621,.F.);
#4879=ADVANCED_FACE('',(#924),#622,.F.);
#4880=ADVANCED_FACE('',(#925),#623,.F.);
#4881=ADVANCED_FACE('',(#926),#624,.F.);
#4882=ADVANCED_FACE('',(#927),#625,.F.);
#4932=CLOSED_SHELL('',(#4866,#4867,#4868,#4869,#4870,#4871,#4872,#4873,
#4874));
#4933=CLOSED_SHELL('',(#4875,#4876,#4877,#4878,#4879,#4880,#4881,#4882));
#5792=AXIS2_PLACEMENT_3D('',#10400,#7283,#7284);
#5793=AXIS2_PLACEMENT_3D('',#10401,#7285,#7286);
#5794=AXIS2_PLACEMENT_3D('',#10403,#7287,#7288);
#5795=AXIS2_PLACEMENT_3D('',#10404,#7289,#7290);
#5796=AXIS2_PLACEMENT_3D('',#10406,#7291,#7292);
#5797=AXIS2_PLACEMENT_3D('',#10408,#7294,#7295);
#5798=AXIS2_PLACEMENT_3D('',#10410,#7296,#7297);
#5799=AXIS2_PLACEMENT_3D('',#10412,#7299,#7300);
#5800=AXIS2_PLACEMENT_3D('',#10414,#7301,#7302);
#5801=AXIS2_PLACEMENT_3D('',#10416,#7304,#7305);
#5802=AXIS2_PLACEMENT_3D('',#10418,#7306,#7307);
#5803=AXIS2_PLACEMENT_3D('',#10419,#7308,#7309);
#5804=AXIS2_PLACEMENT_3D('',#10421,#7310,#7311);
#5805=AXIS2_PLACEMENT_3D('',#10423,#7313,#7314);
#5806=AXIS2_PLACEMENT_3D('',#10425,#7315,#7316);
#5807=AXIS2_PLACEMENT_3D('',#10427,#7318,#7319);
#5808=AXIS2_PLACEMENT_3D('',#10429,#7320,#7321);
#5809=AXIS2_PLACEMENT_3D('',#10431,#7323,#7324);
#5810=AXIS2_PLACEMENT_3D('',#10432,#7325,#7326);
#5811=AXIS2_PLACEMENT_3D('',#10441,#7331,#7332);
#5812=AXIS2_PLACEMENT_3D('',#10447,#7336,#7337);
#5813=AXIS2_PLACEMENT_3D('',#10453,#7341,#7342);
#5814=AXIS2_PLACEMENT_3D('',#10459,#7346,#7347);
#5815=AXIS2_PLACEMENT_3D('',#10465,#7351,#7352);
#5816=AXIS2_PLACEMENT_3D('',#10468,#7355,#7356);
#5817=AXIS2_PLACEMENT_3D('',#10469,#7357,#7358);
#7283=DIRECTION('axis',(0.,0.,1.));
#7284=DIRECTION('refdir',(1.,0.,0.));
#7285=DIRECTION('center_axis',(0.,1.,0.));
#7286=DIRECTION('ref_axis',(0.,0.,1.));
#7287=DIRECTION('center_axis',(0.,-1.,0.));
#7288=DIRECTION('ref_axis',(1.,0.,0.));
#7289=DIRECTION('center_axis',(0.,-1.,0.));
#7290=DIRECTION('ref_axis',(1.,0.,0.));
#7291=DIRECTION('center_axis',(0.,-1.,0.));
#7292=DIRECTION('ref_axis',(1.,0.,0.));
#7293=DIRECTION('',(0.707106781186547,0.707106781186548,8.65956056235493E-17));
#7294=DIRECTION('center_axis',(0.,-1.,0.));
#7295=DIRECTION('ref_axis',(1.,0.,0.));
#7296=DIRECTION('center_axis',(0.,-1.,0.));
#7297=DIRECTION('ref_axis',(1.,0.,0.));
#7298=DIRECTION('',(0.,1.,0.));
#7299=DIRECTION('center_axis',(0.,1.,0.));
#7300=DIRECTION('ref_axis',(1.,0.,0.));
#7301=DIRECTION('center_axis',(0.,-1.,0.));
#7302=DIRECTION('ref_axis',(1.,0.,0.));
#7303=DIRECTION('',(-0.707106781186547,0.707106781186548,-8.65956056235493E-17));
#7304=DIRECTION('center_axis',(0.,-1.,0.));
#7305=DIRECTION('ref_axis',(0.,0.,-1.));
#7306=DIRECTION('center_axis',(0.,-1.,0.));
#7307=DIRECTION('ref_axis',(1.,0.,0.));
#7308=DIRECTION('center_axis',(0.,1.,0.));
#7309=DIRECTION('ref_axis',(1.,0.,0.));
#7310=DIRECTION('center_axis',(0.,1.,0.));
#7311=DIRECTION('ref_axis',(1.,0.,0.));
#7312=DIRECTION('',(-0.447213595499958,0.894427190999916,-5.47678698264203E-17));
#7313=DIRECTION('center_axis',(0.,-1.,0.));
#7314=DIRECTION('ref_axis',(1.,0.,0.));
#7315=DIRECTION('center_axis',(0.,1.,0.));
#7316=DIRECTION('ref_axis',(1.,0.,0.));
#7317=DIRECTION('',(0.,1.,0.));
#7318=DIRECTION('center_axis',(0.,1.,0.));
#7319=DIRECTION('ref_axis',(1.,0.,0.));
#7320=DIRECTION('center_axis',(0.,-1.,0.));
#7321=DIRECTION('ref_axis',(1.,0.,0.));
#7322=DIRECTION('',(-0.707106781186547,0.707106781186548,-8.65956056235493E-17));
#7323=DIRECTION('center_axis',(0.,-1.,0.));
#7324=DIRECTION('ref_axis',(0.,0.,-1.));
#7325=DIRECTION('center_axis',(0.866025403784439,0.,-0.5));
#7326=DIRECTION('ref_axis',(0.5,0.,0.866025403784439));
#7327=DIRECTION('',(-0.5,0.,-0.866025403784439));
#7328=DIRECTION('',(0.,-1.,0.));
#7329=DIRECTION('',(0.5,0.,0.866025403784439));
#7330=DIRECTION('',(0.,-1.,0.));
#7331=DIRECTION('center_axis',(1.60246890531964E-16,0.,-1.));
#7332=DIRECTION('ref_axis',(1.,0.,1.60246890531964E-16));
#7333=DIRECTION('',(-1.,0.,-1.60246890531964E-16));
#7334=DIRECTION('',(0.,-1.,0.));
#7335=DIRECTION('',(1.,0.,1.60246890531964E-16));
#7336=DIRECTION('center_axis',(-0.866025403784439,0.,-0.5));
#7337=DIRECTION('ref_axis',(0.5,0.,-0.866025403784439));
#7338=DIRECTION('',(-0.5,0.,0.866025403784439));
#7339=DIRECTION('',(0.,-1.,0.));
#7340=DIRECTION('',(0.5,0.,-0.866025403784439));
#7341=DIRECTION('center_axis',(-0.866025403784439,0.,0.5));
#7342=DIRECTION('ref_axis',(-0.5,0.,-0.866025403784439));
#7343=DIRECTION('',(0.5,0.,0.866025403784439));
#7344=DIRECTION('',(0.,-1.,0.));
#7345=DIRECTION('',(-0.5,0.,-0.866025403784439));
#7346=DIRECTION('center_axis',(-1.60246890531964E-16,0.,1.));
#7347=DIRECTION('ref_axis',(-1.,0.,-1.60246890531964E-16));
#7348=DIRECTION('',(1.,0.,1.60246890531964E-16));
#7349=DIRECTION('',(0.,-1.,0.));
#7350=DIRECTION('',(-1.,0.,-1.60246890531964E-16));
#7351=DIRECTION('center_axis',(0.866025403784439,0.,0.5));
#7352=DIRECTION('ref_axis',(-0.5,0.,0.866025403784439));
#7353=DIRECTION('',(0.5,0.,-0.866025403784439));
#7354=DIRECTION('',(-0.5,0.,0.866025403784439));
#7355=DIRECTION('center_axis',(0.,1.,0.));
#7356=DIRECTION('ref_axis',(1.,0.,0.));
#7357=DIRECTION('center_axis',(0.,-1.,0.));
#7358=DIRECTION('ref_axis',(0.,0.,-1.));
#10400=CARTESIAN_POINT('',(0.,0.,0.));
#10401=CARTESIAN_POINT('Origin',(0.3,0.4,0.));
#10402=CARTESIAN_POINT('',(-0.3,0.4,-3.67394039744206E-17));
#10403=CARTESIAN_POINT('Origin',(0.,0.4,0.));
#10404=CARTESIAN_POINT('Origin',(0.,0.375,0.));
#10405=CARTESIAN_POINT('',(-0.35,0.35,-4.28626379701573E-17));
#10406=CARTESIAN_POINT('Origin',(0.,0.35,0.));
#10407=CARTESIAN_POINT('',(-0.325,0.375,-3.9801020972289E-17));
#10408=CARTESIAN_POINT('Origin',(0.,0.19,0.));
#10409=CARTESIAN_POINT('',(-0.35,0.03,-4.28626379701574E-17));
#10410=CARTESIAN_POINT('Origin',(0.,0.03,0.));
#10411=CARTESIAN_POINT('',(-0.35,0.19,-4.28626379701574E-17));
#10412=CARTESIAN_POINT('Origin',(0.,0.0149999999999999,0.));
#10413=CARTESIAN_POINT('',(-0.32,-3.29597460435593E-17,-3.91886975727153E-17));
#10414=CARTESIAN_POINT('Origin',(0.,0.,0.));
#10415=CARTESIAN_POINT('',(-0.335,0.0149999999999999,-4.10256677714363E-17));
#10416=CARTESIAN_POINT('Origin',(0.22,0.,0.));
#10417=CARTESIAN_POINT('',(-0.22,-6.93889390390723E-18,-2.69422295812418E-17));
#10418=CARTESIAN_POINT('Origin',(0.,0.,0.));
#10419=CARTESIAN_POINT('Origin',(0.,-0.02,0.));
#10420=CARTESIAN_POINT('',(-0.1954,-0.0492,2.39295984553393E-17));
#10421=CARTESIAN_POINT('Origin',(0.,-0.0492,0.));
#10422=CARTESIAN_POINT('',(-0.21,-0.02,-2.57175827820944E-17));
#10423=CARTESIAN_POINT('Origin',(0.,-0.8,0.));
#10424=CARTESIAN_POINT('',(-0.1954,-1.5646,2.39295984553393E-17));
#10425=CARTESIAN_POINT('Origin',(0.,-1.5646,0.));
#10426=CARTESIAN_POINT('',(-0.1954,-0.8,-2.39295984553393E-17));
#10427=CARTESIAN_POINT('Origin',(0.,-1.58,0.));
#10428=CARTESIAN_POINT('',(-0.16,-1.6,-1.95943487863577E-17));
#10429=CARTESIAN_POINT('Origin',(0.,-1.6,0.));
#10430=CARTESIAN_POINT('',(-0.18,-1.58,-2.20436423846524E-17));
#10431=CARTESIAN_POINT('Origin',(0.,-1.6,0.));
#10432=CARTESIAN_POINT('Origin',(0.0866025403784439,-0.4,-0.15));
#10433=CARTESIAN_POINT('',(0.173205080756888,-0.4,0.));
#10434=CARTESIAN_POINT('',(0.0866025403784439,-0.4,-0.15));
#10435=CARTESIAN_POINT('',(0.173205080756888,-0.4,0.));
#10436=CARTESIAN_POINT('',(0.0866025403784439,-0.64,-0.15));
#10437=CARTESIAN_POINT('',(0.0866025403784439,-0.4,-0.15));
#10438=CARTESIAN_POINT('',(0.173205080756888,-0.64,0.));
#10439=CARTESIAN_POINT('',(0.173205080756888,-0.64,0.));
#10440=CARTESIAN_POINT('',(0.173205080756888,-0.4,0.));
#10441=CARTESIAN_POINT('Origin',(-0.0866025403784438,-0.4,-0.15));
#10442=CARTESIAN_POINT('',(-0.0866025403784438,-0.4,-0.15));
#10443=CARTESIAN_POINT('',(0.0866025403784439,-0.4,-0.15));
#10444=CARTESIAN_POINT('',(-0.0866025403784438,-0.64,-0.15));
#10445=CARTESIAN_POINT('',(-0.0866025403784438,-0.4,-0.15));
#10446=CARTESIAN_POINT('',(0.0866025403784439,-0.64,-0.15));
#10447=CARTESIAN_POINT('Origin',(-0.173205080756888,-0.4,-2.77555756156289E-17));
#10448=CARTESIAN_POINT('',(-0.173205080756888,-0.4,-2.12115047744981E-17));
#10449=CARTESIAN_POINT('',(-0.0866025403784438,-0.4,-0.15));
#10450=CARTESIAN_POINT('',(-0.173205080756888,-0.64,-2.77555756156289E-17));
#10451=CARTESIAN_POINT('',(-0.173205080756888,-0.4,-2.12115047744981E-17));
#10452=CARTESIAN_POINT('',(-0.0866025403784438,-0.64,-0.15));
#10453=CARTESIAN_POINT('Origin',(-0.0866025403784439,-0.4,0.15));
#10454=CARTESIAN_POINT('',(-0.0866025403784439,-0.4,0.15));
#10455=CARTESIAN_POINT('',(-0.173205080756888,-0.4,-2.12115047744981E-17));
#10456=CARTESIAN_POINT('',(-0.0866025403784439,-0.64,0.15));
#10457=CARTESIAN_POINT('',(-0.0866025403784439,-0.4,0.15));
#10458=CARTESIAN_POINT('',(-0.173205080756888,-0.64,-2.12115047744981E-17));
#10459=CARTESIAN_POINT('Origin',(0.0866025403784439,-0.4,0.15));
#10460=CARTESIAN_POINT('',(0.0866025403784439,-0.4,0.15));
#10461=CARTESIAN_POINT('',(-0.0866025403784439,-0.4,0.15));
#10462=CARTESIAN_POINT('',(0.0866025403784439,-0.64,0.15));
#10463=CARTESIAN_POINT('',(0.0866025403784439,-0.4,0.15));
#10464=CARTESIAN_POINT('',(-0.0866025403784439,-0.64,0.15));
#10465=CARTESIAN_POINT('Origin',(0.173205080756888,-0.4,0.));
#10466=CARTESIAN_POINT('',(0.0866025403784439,-0.4,0.15));
#10467=CARTESIAN_POINT('',(0.0866025403784439,-0.64,0.15));
#10468=CARTESIAN_POINT('Origin',(0.,-0.4,-2.77555756156289E-17));
#10469=CARTESIAN_POINT('Origin',(0.,-0.64,-2.77555756156289E-17));
#10593=UNCERTAINTY_MEASURE_WITH_UNIT(LENGTH_MEASURE(0.001),#10628,
'DISTANCE_ACCURACY_VALUE',
'Maximum model space distance between geometric entities at asserted c
onnectivities');
#10595=UNCERTAINTY_MEASURE_WITH_UNIT(LENGTH_MEASURE(0.001),#10628,
'DISTANCE_ACCURACY_VALUE',
'Maximum model space distance between geometric entities at asserted c
onnectivities');
#10625=(
GEOMETRIC_REPRESENTATION_CONTEXT(3)
GLOBAL_UNCERTAINTY_ASSIGNED_CONTEXT((#10593))
GLOBAL_UNIT_ASSIGNED_CONTEXT((#10628,#10630,#10631))
REPRESENTATION_CONTEXT('','3D')
);
#10627=(
GEOMETRIC_REPRESENTATION_CONTEXT(3)
GLOBAL_UNCERTAINTY_ASSIGNED_CONTEXT((#10595))
GLOBAL_UNIT_ASSIGNED_CONTEXT((#10628,#10630,#10631))
REPRESENTATION_CONTEXT('','3D')
);
#10628=(
LENGTH_UNIT()
NAMED_UNIT(*)
SI_UNIT(.CENTI.,.METRE.)
);
#10630=(
NAMED_UNIT(*)
PLANE_ANGLE_UNIT()
SI_UNIT($,.RADIAN.)
);
#10631=(
NAMED_UNIT(*)
SI_UNIT($,.STERADIAN.)
SOLID_ANGLE_UNIT()
);
#10661=SHAPE_DEFINITION_REPRESENTATION(#10707,#10766);
#10707=PRODUCT_DEFINITION_SHAPE('',$,#10798);
#10766=SHAPE_REPRESENTATION('',(#5792),#10625);
#10768=PRODUCT_DEFINITION_CONTEXT('part definition',#10863,'design');
#10798=PRODUCT_DEFINITION('Cap Screw - M4x16','Cap Screw - M4x16',#10829,
#10768);
#10829=PRODUCT_DEFINITION_FORMATION('',$,#10894);
#10863=APPLICATION_CONTEXT(
'Core Data for Automotive Mechanical Design Process');
#10864=PRODUCT_CONTEXT('part definition',#10863,'mechanical');
#10894=PRODUCT('Cap Screw - M4x16','Cap Screw - M4x16',
'Cap Screw - M4x16',(#10864));
#10966=COLOUR_RGB('Black',0.12,0.14,0.17);
#10967=FILL_AREA_STYLE_COLOUR('',#10966);
#10968=FILL_AREA_STYLE('',(#10967));
#10969=SURFACE_STYLE_FILL_AREA(#10968);
#10970=SURFACE_SIDE_STYLE('',(#10969));
#10971=SURFACE_STYLE_USAGE(.BOTH.,#10970);
#10972=PRESENTATION_STYLE_ASSIGNMENT((#10971));
ENDSEC;
END-ISO-10303-21;
